ISO-10303-21;
HEADER;
/* Generated by software containing ST-Developer
 * from STEP Tools, Inc. (www.steptools.com) 
 */

FILE_DESCRIPTION(
/* description */ ('Bin tilter linkage'),
/* implementation_level */ '2;1');

FILE_NAME(
/* name */ 'Bearing cap (2).step',
/* time_stamp */ '2026-10-28T03:26:24-07:00',
/* author */ (''),
/* organization */ (''),
/* preprocessor_version */ 'ST-DEVELOPER v20.2',
/* originating_system */ 'Autodesk Translation Framework v15.17.0.0',
/* authorisation */ '');

FILE_SCHEMA (('AUTOMOTIVE_DESIGN { 1 0 10303 214 3 1 1 }'));
ENDSEC;

DATA;
#10=MECHANICAL_DESIGN_GEOMETRIC_PRESENTATION_REPRESENTATION('',(#903),#23728);
#691=SHAPE_REPRESENTATION_RELATIONSHIP('SRR','None',#24156,#797);
#797=ADVANCED_BREP_SHAPE_REPRESENTATION('',(#1016),#23656);
#903=STYLED_ITEM('',(#24765),#1016);
#1016=MANIFOLD_SOLID_BREP('Body1',#12434);
#1282=FACE_BOUND('',#3190,.T.);
#1283=FACE_BOUND('',#3191,.T.);
#1284=FACE_BOUND('',#3192,.T.);
#1285=FACE_BOUND('',#3193,.T.);
#1286=FACE_BOUND('',#3194,.T.);
#1287=FACE_BOUND('',#3196,.T.);
#1288=FACE_BOUND('',#3197,.T.);
#1289=FACE_BOUND('',#3198,.T.);
#1290=FACE_BOUND('',#3199,.T.);
#1291=FACE_BOUND('',#3200,.T.);
#1649=PLANE('',#14384);
#1650=PLANE('',#14385);
#2211=FACE_OUTER_BOUND('',#3183,.T.);
#2212=FACE_OUTER_BOUND('',#3184,.T.);
#2213=FACE_OUTER_BOUND('',#3185,.T.);
#2214=FACE_OUTER_BOUND('',#3186,.T.);
#2215=FACE_OUTER_BOUND('',#3187,.T.);
#2216=FACE_OUTER_BOUND('',#3188,.T.);
#2217=FACE_OUTER_BOUND('',#3189,.T.);
#2218=FACE_OUTER_BOUND('',#3195,.T.);
#3183=EDGE_LOOP('',(#9625,#9626,#9627,#9628));
#3184=EDGE_LOOP('',(#9629,#9630,#9631,#9632));
#3185=EDGE_LOOP('',(#9633,#9634,#9635,#9636));
#3186=EDGE_LOOP('',(#9637,#9638,#9639,#9640));
#3187=EDGE_LOOP('',(#9641,#9642,#9643,#9644));
#3188=EDGE_LOOP('',(#9645,#9646,#9647,#9648));
#3189=EDGE_LOOP('',(#9649));
#3190=EDGE_LOOP('',(#9650));
#3191=EDGE_LOOP('',(#9651));
#3192=EDGE_LOOP('',(#9652));
#3193=EDGE_LOOP('',(#9653));
#3194=EDGE_LOOP('',(#9654));
#3195=EDGE_LOOP('',(#9655));
#3196=EDGE_LOOP('',(#9656));
#3197=EDGE_LOOP('',(#9657));
#3198=EDGE_LOOP('',(#9658));
#3199=EDGE_LOOP('',(#9659));
#3200=EDGE_LOOP('',(#9660));
#4151=LINE('',#21157,#4826);
#4152=LINE('',#21163,#4827);
#4153=LINE('',#21169,#4828);
#4154=LINE('',#21175,#4829);
#4155=LINE('',#21181,#4830);
#4156=LINE('',#21187,#4831);
#4826=VECTOR('',#17160,0.225);
#4827=VECTOR('',#17167,0.225);
#4828=VECTOR('',#17174,0.225);
#4829=VECTOR('',#17181,0.225);
#4830=VECTOR('',#17188,1.02);
#4831=VECTOR('',#17195,2.2);
#5523=CIRCLE('',#14367,0.225);
#5524=CIRCLE('',#14368,0.225);
#5525=CIRCLE('',#14370,0.225);
#5526=CIRCLE('',#14371,0.225);
#5527=CIRCLE('',#14373,0.225);
#5528=CIRCLE('',#14374,0.225);
#5529=CIRCLE('',#14376,0.225);
#5530=CIRCLE('',#14377,0.225);
#5531=CIRCLE('',#14379,1.02);
#5532=CIRCLE('',#14380,1.02);
#5533=CIRCLE('',#14382,2.2);
#5534=CIRCLE('',#14383,2.2);
#6373=VERTEX_POINT('',#21154);
#6374=VERTEX_POINT('',#21156);
#6375=VERTEX_POINT('',#21160);
#6376=VERTEX_POINT('',#21162);
#6377=VERTEX_POINT('',#21166);
#6378=VERTEX_POINT('',#21168);
#6379=VERTEX_POINT('',#21172);
#6380=VERTEX_POINT('',#21174);
#6381=VERTEX_POINT('',#21178);
#6382=VERTEX_POINT('',#21180);
#6383=VERTEX_POINT('',#21184);
#6384=VERTEX_POINT('',#21186);
#7552=EDGE_CURVE('',#6373,#6373,#5523,.T.);
#7553=EDGE_CURVE('',#6373,#6374,#4151,.T.);
#7554=EDGE_CURVE('',#6374,#6374,#5524,.T.);
#7555=EDGE_CURVE('',#6375,#6375,#5525,.T.);
#7556=EDGE_CURVE('',#6375,#6376,#4152,.T.);
#7557=EDGE_CURVE('',#6376,#6376,#5526,.T.);
#7558=EDGE_CURVE('',#6377,#6377,#5527,.T.);
#7559=EDGE_CURVE('',#6377,#6378,#4153,.T.);
#7560=EDGE_CURVE('',#6378,#6378,#5528,.T.);
#7561=EDGE_CURVE('',#6379,#6379,#5529,.T.);
#7562=EDGE_CURVE('',#6379,#6380,#4154,.T.);
#7563=EDGE_CURVE('',#6380,#6380,#5530,.T.);
#7564=EDGE_CURVE('',#6381,#6381,#5531,.T.);
#7565=EDGE_CURVE('',#6381,#6382,#4155,.T.);
#7566=EDGE_CURVE('',#6382,#6382,#5532,.T.);
#7567=EDGE_CURVE('',#6383,#6383,#5533,.T.);
#7568=EDGE_CURVE('',#6383,#6384,#4156,.T.);
#7569=EDGE_CURVE('',#6384,#6384,#5534,.T.);
#9625=ORIENTED_EDGE('',*,*,#7552,.F.);
#9626=ORIENTED_EDGE('',*,*,#7553,.T.);
#9627=ORIENTED_EDGE('',*,*,#7554,.F.);
#9628=ORIENTED_EDGE('',*,*,#7553,.F.);
#9629=ORIENTED_EDGE('',*,*,#7555,.F.);
#9630=ORIENTED_EDGE('',*,*,#7556,.T.);
#9631=ORIENTED_EDGE('',*,*,#7557,.F.);
#9632=ORIENTED_EDGE('',*,*,#7556,.F.);
#9633=ORIENTED_EDGE('',*,*,#7558,.F.);
#9634=ORIENTED_EDGE('',*,*,#7559,.T.);
#9635=ORIENTED_EDGE('',*,*,#7560,.F.);
#9636=ORIENTED_EDGE('',*,*,#7559,.F.);
#9637=ORIENTED_EDGE('',*,*,#7561,.F.);
#9638=ORIENTED_EDGE('',*,*,#7562,.T.);
#9639=ORIENTED_EDGE('',*,*,#7563,.F.);
#9640=ORIENTED_EDGE('',*,*,#7562,.F.);
#9641=ORIENTED_EDGE('',*,*,#7564,.F.);
#9642=ORIENTED_EDGE('',*,*,#7565,.T.);
#9643=ORIENTED_EDGE('',*,*,#7566,.T.);
#9644=ORIENTED_EDGE('',*,*,#7565,.F.);
#9645=ORIENTED_EDGE('',*,*,#7567,.F.);
#9646=ORIENTED_EDGE('',*,*,#7568,.T.);
#9647=ORIENTED_EDGE('',*,*,#7569,.T.);
#9648=ORIENTED_EDGE('',*,*,#7568,.F.);
#9649=ORIENTED_EDGE('',*,*,#7567,.T.);
#9650=ORIENTED_EDGE('',*,*,#7564,.T.);
#9651=ORIENTED_EDGE('',*,*,#7563,.T.);
#9652=ORIENTED_EDGE('',*,*,#7560,.T.);
#9653=ORIENTED_EDGE('',*,*,#7557,.T.);
#9654=ORIENTED_EDGE('',*,*,#7554,.T.);
#9655=ORIENTED_EDGE('',*,*,#7569,.F.);
#9656=ORIENTED_EDGE('',*,*,#7566,.F.);
#9657=ORIENTED_EDGE('',*,*,#7561,.T.);
#9658=ORIENTED_EDGE('',*,*,#7558,.T.);
#9659=ORIENTED_EDGE('',*,*,#7555,.T.);
#9660=ORIENTED_EDGE('',*,*,#7552,.T.);
#11427=CYLINDRICAL_SURFACE('',#14366,0.225);
#11428=CYLINDRICAL_SURFACE('',#14369,0.225);
#11429=CYLINDRICAL_SURFACE('',#14372,0.225);
#11430=CYLINDRICAL_SURFACE('',#14375,0.225);
#11431=CYLINDRICAL_SURFACE('',#14378,1.02);
#11432=CYLINDRICAL_SURFACE('',#14381,2.2);
#11936=ADVANCED_FACE('',(#2211),#11427,.F.);
#11937=ADVANCED_FACE('',(#2212),#11428,.F.);
#11938=ADVANCED_FACE('',(#2213),#11429,.F.);
#11939=ADVANCED_FACE('',(#2214),#11430,.F.);
#11940=ADVANCED_FACE('',(#2215),#11431,.F.);
#11941=ADVANCED_FACE('',(#2216),#11432,.T.);
#11942=ADVANCED_FACE('',(#2217,#1282,#1283,#1284,#1285,#1286),#1649,.T.);
#11943=ADVANCED_FACE('',(#2218,#1287,#1288,#1289,#1290,#1291),#1650,.F.);
#12434=CLOSED_SHELL('',(#11936,#11937,#11938,#11939,#11940,#11941,#11942,
#11943));
#14365=AXIS2_PLACEMENT_3D('',#21152,#17154,#17155);
#14366=AXIS2_PLACEMENT_3D('',#21153,#17156,#17157);
#14367=AXIS2_PLACEMENT_3D('',#21155,#17158,#17159);
#14368=AXIS2_PLACEMENT_3D('',#21158,#17161,#17162);
#14369=AXIS2_PLACEMENT_3D('',#21159,#17163,#17164);
#14370=AXIS2_PLACEMENT_3D('',#21161,#17165,#17166);
#14371=AXIS2_PLACEMENT_3D('',#21164,#17168,#17169);
#14372=AXIS2_PLACEMENT_3D('',#21165,#17170,#17171);
#14373=AXIS2_PLACEMENT_3D('',#21167,#17172,#17173);
#14374=AXIS2_PLACEMENT_3D('',#21170,#17175,#17176);
#14375=AXIS2_PLACEMENT_3D('',#21171,#17177,#17178);
#14376=AXIS2_PLACEMENT_3D('',#21173,#17179,#17180);
#14377=AXIS2_PLACEMENT_3D('',#21176,#17182,#17183);
#14378=AXIS2_PLACEMENT_3D('',#21177,#17184,#17185);
#14379=AXIS2_PLACEMENT_3D('',#21179,#17186,#17187);
#14380=AXIS2_PLACEMENT_3D('',#21182,#17189,#17190);
#14381=AXIS2_PLACEMENT_3D('',#21183,#17191,#17192);
#14382=AXIS2_PLACEMENT_3D('',#21185,#17193,#17194);
#14383=AXIS2_PLACEMENT_3D('',#21188,#17196,#17197);
#14384=AXIS2_PLACEMENT_3D('',#21189,#17198,#17199);
#14385=AXIS2_PLACEMENT_3D('',#21190,#17200,#17201);
#17154=DIRECTION('axis',(0.,0.,1.));
#17155=DIRECTION('refdir',(1.,0.,0.));
#17156=DIRECTION('center_axis',(0.,1.,0.));
#17157=DIRECTION('ref_axis',(1.,0.,0.));
#17158=DIRECTION('center_axis',(0.,1.,0.));
#17159=DIRECTION('ref_axis',(1.,0.,0.));
#17160=DIRECTION('',(0.,1.,0.));
#17161=DIRECTION('center_axis',(0.,-1.,0.));
#17162=DIRECTION('ref_axis',(1.,0.,0.));
#17163=DIRECTION('center_axis',(0.,1.,0.));
#17164=DIRECTION('ref_axis',(1.,0.,0.));
#17165=DIRECTION('center_axis',(0.,1.,0.));
#17166=DIRECTION('ref_axis',(1.,0.,0.));
#17167=DIRECTION('',(0.,1.,0.));
#17168=DIRECTION('center_axis',(0.,-1.,0.));
#17169=DIRECTION('ref_axis',(1.,0.,0.));
#17170=DIRECTION('center_axis',(0.,1.,0.));
#17171=DIRECTION('ref_axis',(1.,0.,0.));
#17172=DIRECTION('center_axis',(0.,1.,0.));
#17173=DIRECTION('ref_axis',(1.,0.,0.));
#17174=DIRECTION('',(0.,1.,0.));
#17175=DIRECTION('center_axis',(0.,-1.,0.));
#17176=DIRECTION('ref_axis',(1.,0.,0.));
#17177=DIRECTION('center_axis',(0.,1.,0.));
#17178=DIRECTION('ref_axis',(1.,0.,0.));
#17179=DIRECTION('center_axis',(0.,1.,0.));
#17180=DIRECTION('ref_axis',(1.,0.,0.));
#17181=DIRECTION('',(0.,1.,0.));
#17182=DIRECTION('center_axis',(0.,-1.,0.));
#17183=DIRECTION('ref_axis',(1.,0.,0.));
#17184=DIRECTION('center_axis',(0.,1.,0.));
#17185=DIRECTION('ref_axis',(1.,0.,0.));
#17186=DIRECTION('center_axis',(0.,-1.,0.));
#17187=DIRECTION('ref_axis',(1.,0.,0.));
#17188=DIRECTION('',(0.,-1.,0.));
#17189=DIRECTION('center_axis',(0.,-1.,0.));
#17190=DIRECTION('ref_axis',(1.,0.,0.));
#17191=DIRECTION('center_axis',(0.,1.,0.));
#17192=DIRECTION('ref_axis',(1.,0.,0.));
#17193=DIRECTION('center_axis',(0.,1.,0.));
#17194=DIRECTION('ref_axis',(1.,0.,0.));
#17195=DIRECTION('',(0.,-1.,0.));
#17196=DIRECTION('center_axis',(0.,1.,0.));
#17197=DIRECTION('ref_axis',(1.,0.,0.));
#17198=DIRECTION('center_axis',(0.,1.,0.));
#17199=DIRECTION('ref_axis',(1.,0.,0.));
#17200=DIRECTION('center_axis',(0.,1.,0.));
#17201=DIRECTION('ref_axis',(1.,0.,0.));
#21152=CARTESIAN_POINT('',(0.,0.,0.));
#21153=CARTESIAN_POINT('Origin',(8.08877866266397,-0.9,17.1120538880616));
#21154=CARTESIAN_POINT('',(7.86377866266397,-0.8,17.1120538880616));
#21155=CARTESIAN_POINT('Origin',(8.08877866266397,-0.8,17.1120538880616));
#21156=CARTESIAN_POINT('',(7.86377866266397,-0.5,17.1120538880616));
#21157=CARTESIAN_POINT('',(7.86377866266397,-0.9,17.1120538880616));
#21158=CARTESIAN_POINT('Origin',(8.08877866266397,-0.5,17.1120538880616));
#21159=CARTESIAN_POINT('Origin',(8.08877866266397,-0.9,19.7283489784518));
#21160=CARTESIAN_POINT('',(7.86377866266397,-0.8,19.7283489784518));
#21161=CARTESIAN_POINT('Origin',(8.08877866266397,-0.8,19.7283489784518));
#21162=CARTESIAN_POINT('',(7.86377866266397,-0.5,19.7283489784518));
#21163=CARTESIAN_POINT('',(7.86377866266397,-0.9,19.7283489784518));
#21164=CARTESIAN_POINT('Origin',(8.08877866266397,-0.5,19.7283489784518));
#21165=CARTESIAN_POINT('Origin',(10.7050737530542,-0.9,19.7283489784518));
#21166=CARTESIAN_POINT('',(10.4800737530542,-0.8,19.7283489784518));
#21167=CARTESIAN_POINT('Origin',(10.7050737530542,-0.8,19.7283489784518));
#21168=CARTESIAN_POINT('',(10.4800737530542,-0.5,19.7283489784518));
#21169=CARTESIAN_POINT('',(10.4800737530542,-0.9,19.7283489784518));
#21170=CARTESIAN_POINT('Origin',(10.7050737530542,-0.5,19.7283489784518));
#21171=CARTESIAN_POINT('Origin',(10.7050737530542,-0.9,17.1120538880616));
#21172=CARTESIAN_POINT('',(10.4800737530542,-0.8,17.1120538880616));
#21173=CARTESIAN_POINT('Origin',(10.7050737530542,-0.8,17.1120538880616));
#21174=CARTESIAN_POINT('',(10.4800737530542,-0.5,17.1120538880616));
#21175=CARTESIAN_POINT('',(10.4800737530542,-0.9,17.1120538880616));
#21176=CARTESIAN_POINT('Origin',(10.7050737530542,-0.5,17.1120538880616));
#21177=CARTESIAN_POINT('Origin',(9.39692620785909,-0.8,18.4202014332567));
#21178=CARTESIAN_POINT('',(8.37692620785909,-0.5,18.4202014332567));
#21179=CARTESIAN_POINT('Origin',(9.39692620785909,-0.5,18.4202014332567));
#21180=CARTESIAN_POINT('',(8.37692620785909,-0.8,18.4202014332567));
#21181=CARTESIAN_POINT('',(8.37692620785909,-0.8,18.4202014332567));
#21182=CARTESIAN_POINT('Origin',(9.39692620785909,-0.8,18.4202014332567));
#21183=CARTESIAN_POINT('Origin',(9.39692620785909,-0.8,18.4202014332567));
#21184=CARTESIAN_POINT('',(7.19692620785909,-0.5,18.4202014332567));
#21185=CARTESIAN_POINT('Origin',(9.39692620785909,-0.5,18.4202014332567));
#21186=CARTESIAN_POINT('',(7.19692620785909,-0.8,18.4202014332567));
#21187=CARTESIAN_POINT('',(7.19692620785909,-0.8,18.4202014332567));
#21188=CARTESIAN_POINT('Origin',(9.39692620785909,-0.8,18.4202014332567));
#21189=CARTESIAN_POINT('Origin',(9.39692620785909,-0.5,18.4202014332567));
#21190=CARTESIAN_POINT('Origin',(9.39692620785909,-0.8,18.4202014332567));
#23539=UNCERTAINTY_MEASURE_WITH_UNIT(LENGTH_MEASURE(0.001),#23729,
'DISTANCE_ACCURACY_VALUE',
'Maximum model space distance between geometric entities at asserted c
onnectivities');
#23611=UNCERTAINTY_MEASURE_WITH_UNIT(LENGTH_MEASURE(0.001),#23729,
'DISTANCE_ACCURACY_VALUE',
'Maximum model space distance between geometric entities at asserted c
onnectivities');
#23656=(
GEOMETRIC_REPRESENTATION_CONTEXT(3)
GLOBAL_UNCERTAINTY_ASSIGNED_CONTEXT((#23539))
GLOBAL_UNIT_ASSIGNED_CONTEXT((#23729,#23731,#23732))
REPRESENTATION_CONTEXT('','3D')
);
#23728=(
GEOMETRIC_REPRESENTATION_CONTEXT(3)
GLOBAL_UNCERTAINTY_ASSIGNED_CONTEXT((#23611))
GLOBAL_UNIT_ASSIGNED_CONTEXT((#23729,#23731,#23732))
REPRESENTATION_CONTEXT('','3D')
);
#23729=(
LENGTH_UNIT()
NAMED_UNIT(*)
SI_UNIT(.CENTI.,.METRE.)
);
#23731=(
NAMED_UNIT(*)
PLANE_ANGLE_UNIT()
SI_UNIT($,.RADIAN.)
);
#23732=(
NAMED_UNIT(*)
SI_UNIT($,.STERADIAN.)
SOLID_ANGLE_UNIT()
);
#23777=SHAPE_DEFINITION_REPRESENTATION(#23893,#24156);
#23893=PRODUCT_DEFINITION_SHAPE('',$,#24273);
#24156=SHAPE_REPRESENTATION('',(#14365),#23656);
#24228=PRODUCT_DEFINITION_CONTEXT('part definition',#24578,'design');
#24273=PRODUCT_DEFINITION('Bearing cap (2)','Bearing cap (2)',#24389,#24228);
#24389=PRODUCT_DEFINITION_FORMATION('',$,#24624);
#24578=APPLICATION_CONTEXT(
'Core Data for Automotive Mechanical Design Process');
#24579=PRODUCT_CONTEXT('part definition',#24578,'mechanical');
#24624=PRODUCT('Bearing cap (2)','Bearing cap (2)','Bearing cap (2)',(#24579));
#24759=COLOUR_RGB('Grey',0.48,0.52,0.57);
#24760=FILL_AREA_STYLE_COLOUR('',#24759);
#24761=FILL_AREA_STYLE('',(#24760));
#24762=SURFACE_STYLE_FILL_AREA(#24761);
#24763=SURFACE_SIDE_STYLE('',(#24762));
#24764=SURFACE_STYLE_USAGE(.BOTH.,#24763);
#24765=PRESENTATION_STYLE_ASSIGNMENT((#24764));
ENDSEC;
END-ISO-10303-21;
